ISO-10303-21;
HEADER;
/* Generated by software containing ST-Developer
 * from STEP Tools, Inc. (www.steptools.com) 
 */

FILE_DESCRIPTION(
/* description */ ('Bin tilter linkage'),
/* implementation_level */ '2;1');

FILE_NAME(
/* name */ 'M4 short cap screw (2).step',
/* time_stamp */ '2026-10-28T03:26:24-07:00',
/* author */ (''),
/* organization */ (''),
/* preprocessor_version */ 'ST-DEVELOPER v20.2',
/* originating_system */ 'Autodesk Translation Framework v15.17.0.0',
/* authorisation */ '');

FILE_SCHEMA (('AUTOMOTIVE_DESIGN { 1 0 10303 214 3 1 1 }'));
ENDSEC;

DATA;
#10=MECHANICAL_DESIGN_GEOMETRIC_PRESENTATION_REPRESENTATION('',(#896),#23728);
#684=SHAPE_REPRESENTATION_RELATIONSHIP('SRR','None',#24149,#790);
#790=ADVANCED_BREP_SHAPE_REPRESENTATION('',(#1009),#23649);
#896=STYLED_ITEM('',(#24772),#1009);
#1009=MANIFOLD_SOLID_BREP('Body1',#12427);
#1266=FACE_BOUND('',#3130,.T.);
#1629=PLANE('',#14285);
#1630=PLANE('',#14290);
#1631=PLANE('',#14293);
#2173=FACE_OUTER_BOUND('',#3129,.T.);
#2174=FACE_OUTER_BOUND('',#3131,.T.);
#2175=FACE_OUTER_BOUND('',#3132,.T.);
#2176=FACE_OUTER_BOUND('',#3133,.T.);
#2177=FACE_OUTER_BOUND('',#3134,.T.);
#3129=EDGE_LOOP('',(#9517));
#3130=EDGE_LOOP('',(#9518));
#3131=EDGE_LOOP('',(#9519,#9520,#9521,#9522));
#3132=EDGE_LOOP('',(#9523));
#3133=EDGE_LOOP('',(#9524,#9525,#9526,#9527));
#3134=EDGE_LOOP('',(#9528));
#4133=LINE('',#21025,#4808);
#4134=LINE('',#21031,#4809);
#4808=VECTOR('',#16984,0.35);
#4809=VECTOR('',#16993,0.2);
#5487=CIRCLE('',#14286,0.35);
#5488=CIRCLE('',#14287,0.2);
#5489=CIRCLE('',#14289,0.35);
#5490=CIRCLE('',#14292,0.2);
#6337=VERTEX_POINT('',#21019);
#6338=VERTEX_POINT('',#21021);
#6339=VERTEX_POINT('',#21024);
#6340=VERTEX_POINT('',#21029);
#7498=EDGE_CURVE('',#6337,#6337,#5487,.T.);
#7499=EDGE_CURVE('',#6338,#6338,#5488,.T.);
#7500=EDGE_CURVE('',#6337,#6339,#4133,.T.);
#7501=EDGE_CURVE('',#6339,#6339,#5489,.T.);
#7502=EDGE_CURVE('',#6340,#6340,#5490,.T.);
#7503=EDGE_CURVE('',#6340,#6338,#4134,.T.);
#9517=ORIENTED_EDGE('',*,*,#7498,.T.);
#9518=ORIENTED_EDGE('',*,*,#7499,.F.);
#9519=ORIENTED_EDGE('',*,*,#7498,.F.);
#9520=ORIENTED_EDGE('',*,*,#7500,.T.);
#9521=ORIENTED_EDGE('',*,*,#7501,.T.);
#9522=ORIENTED_EDGE('',*,*,#7500,.F.);
#9523=ORIENTED_EDGE('',*,*,#7501,.F.);
#9524=ORIENTED_EDGE('',*,*,#7502,.F.);
#9525=ORIENTED_EDGE('',*,*,#7503,.T.);
#9526=ORIENTED_EDGE('',*,*,#7499,.T.);
#9527=ORIENTED_EDGE('',*,*,#7503,.F.);
#9528=ORIENTED_EDGE('',*,*,#7502,.T.);
#11409=CYLINDRICAL_SURFACE('',#14288,0.35);
#11410=CYLINDRICAL_SURFACE('',#14291,0.2);
#11898=ADVANCED_FACE('',(#2173,#1266),#1629,.T.);
#11899=ADVANCED_FACE('',(#2174),#11409,.T.);
#11900=ADVANCED_FACE('',(#2175),#1630,.F.);
#11901=ADVANCED_FACE('',(#2176),#11410,.T.);
#11902=ADVANCED_FACE('',(#2177),#1631,.T.);
#12427=CLOSED_SHELL('',(#11898,#11899,#11900,#11901,#11902));
#14284=AXIS2_PLACEMENT_3D('',#21017,#16974,#16975);
#14285=AXIS2_PLACEMENT_3D('',#21018,#16976,#16977);
#14286=AXIS2_PLACEMENT_3D('',#21020,#16978,#16979);
#14287=AXIS2_PLACEMENT_3D('',#21022,#16980,#16981);
#14288=AXIS2_PLACEMENT_3D('',#21023,#16982,#16983);
#14289=AXIS2_PLACEMENT_3D('',#21026,#16985,#16986);
#14290=AXIS2_PLACEMENT_3D('',#21027,#16987,#16988);
#14291=AXIS2_PLACEMENT_3D('',#21028,#16989,#16990);
#14292=AXIS2_PLACEMENT_3D('',#21030,#16991,#16992);
#14293=AXIS2_PLACEMENT_3D('',#21032,#16994,#16995);
#16974=DIRECTION('axis',(0.,0.,1.));
#16975=DIRECTION('refdir',(1.,0.,0.));
#16976=DIRECTION('center_axis',(0.,1.,0.));
#16977=DIRECTION('ref_axis',(1.,0.,0.));
#16978=DIRECTION('center_axis',(0.,1.,0.));
#16979=DIRECTION('ref_axis',(1.,0.,0.));
#16980=DIRECTION('center_axis',(0.,1.,0.));
#16981=DIRECTION('ref_axis',(1.,0.,0.));
#16982=DIRECTION('center_axis',(0.,1.,0.));
#16983=DIRECTION('ref_axis',(1.,0.,0.));
#16984=DIRECTION('',(0.,-1.,0.));
#16985=DIRECTION('center_axis',(0.,1.,0.));
#16986=DIRECTION('ref_axis',(1.,0.,0.));
#16987=DIRECTION('center_axis',(0.,1.,0.));
#16988=DIRECTION('ref_axis',(1.,0.,0.));
#16989=DIRECTION('center_axis',(0.,1.,0.));
#16990=DIRECTION('ref_axis',(1.,0.,0.));
#16991=DIRECTION('center_axis',(0.,1.,0.));
#16992=DIRECTION('ref_axis',(1.,0.,0.));
#16993=DIRECTION('',(0.,-1.,0.));
#16994=DIRECTION('center_axis',(0.,1.,0.));
#16995=DIRECTION('ref_axis',(1.,0.,0.));
#21017=CARTESIAN_POINT('',(0.,0.,0.));
#21018=CARTESIAN_POINT('Origin',(-1.30814754519511,-0.8,13.6918524548049));
#21019=CARTESIAN_POINT('',(-1.65814754519511,-0.8,13.6918524548049));
#21020=CARTESIAN_POINT('Origin',(-1.30814754519511,-0.8,13.6918524548049));
#21021=CARTESIAN_POINT('',(-1.50814754519511,-0.8,13.6918524548049));
#21022=CARTESIAN_POINT('Origin',(-1.30814754519511,-0.8,13.6918524548049));
#21023=CARTESIAN_POINT('Origin',(-1.30814754519511,-1.2,13.6918524548049));
#21024=CARTESIAN_POINT('',(-1.65814754519511,-1.2,13.6918524548049));
#21025=CARTESIAN_POINT('',(-1.65814754519511,-1.2,13.6918524548049));
#21026=CARTESIAN_POINT('Origin',(-1.30814754519511,-1.2,13.6918524548049));
#21027=CARTESIAN_POINT('Origin',(-1.30814754519511,-1.2,13.6918524548049));
#21028=CARTESIAN_POINT('Origin',(-1.30814754519511,-0.8,13.6918524548049));
#21029=CARTESIAN_POINT('',(-1.50814754519511,-0.1,13.6918524548049));
#21030=CARTESIAN_POINT('Origin',(-1.30814754519511,-0.1,13.6918524548049));
#21031=CARTESIAN_POINT('',(-1.50814754519511,-0.8,13.6918524548049));
#21032=CARTESIAN_POINT('Origin',(-1.30814754519511,-0.1,13.6918524548049));
#23532=UNCERTAINTY_MEASURE_WITH_UNIT(LENGTH_MEASURE(0.001),#23729,
'DISTANCE_ACCURACY_VALUE',
'Maximum model space distance between geometric entities at asserted c
onnectivities');
#23611=UNCERTAINTY_MEASURE_WITH_UNIT(LENGTH_MEASURE(0.001),#23729,
'DISTANCE_ACCURACY_VALUE',
'Maximum model space distance between geometric entities at asserted c
onnectivities');
#23649=(
GEOMETRIC_REPRESENTATION_CONTEXT(3)
GLOBAL_UNCERTAINTY_ASSIGNED_CONTEXT((#23532))
GLOBAL_UNIT_ASSIGNED_CONTEXT((#23729,#23731,#23732))
REPRESENTATION_CONTEXT('','3D')
);
#23728=(
GEOMETRIC_REPRESENTATION_CONTEXT(3)
GLOBAL_UNCERTAINTY_ASSIGNED_CONTEXT((#23611))
GLOBAL_UNIT_ASSIGNED_CONTEXT((#23729,#23731,#23732))
REPRESENTATION_CONTEXT('','3D')
);
#23729=(
LENGTH_UNIT()
NAMED_UNIT(*)
SI_UNIT(.CENTI.,.METRE.)
);
#23731=(
NAMED_UNIT(*)
PLANE_ANGLE_UNIT()
SI_UNIT($,.RADIAN.)
);
#23732=(
NAMED_UNIT(*)
SI_UNIT($,.STERADIAN.)
SOLID_ANGLE_UNIT()
);
#23770=SHAPE_DEFINITION_REPRESENTATION(#23886,#24149);
#23886=PRODUCT_DEFINITION_SHAPE('',$,#24266);
#24149=SHAPE_REPRESENTATION('',(#14284),#23649);
#24228=PRODUCT_DEFINITION_CONTEXT('part definition',#24578,'design');
#24266=PRODUCT_DEFINITION('M4 short cap screw (2)',
'M4 short cap screw (2)',#24382,#24228);
#24382=PRODUCT_DEFINITION_FORMATION('',$,#24617);
#24578=APPLICATION_CONTEXT(
'Core Data for Automotive Mechanical Design Process');
#24579=PRODUCT_CONTEXT('part definition',#24578,'mechanical');
#24617=PRODUCT('M4 short cap screw (2)','M4 short cap screw (2)',
'M4 short cap screw (2)',(#24579));
#24766=COLOUR_RGB('Black',0.12,0.14,0.17);
#24767=FILL_AREA_STYLE_COLOUR('',#24766);
#24768=FILL_AREA_STYLE('',(#24767));
#24769=SURFACE_STYLE_FILL_AREA(#24768);
#24770=SURFACE_SIDE_STYLE('',(#24769));
#24771=SURFACE_STYLE_USAGE(.BOTH.,#24770);
#24772=PRESENTATION_STYLE_ASSIGNMENT((#24771));
ENDSEC;
END-ISO-10303-21;
